ISO-10303-21;
HEADER;
/* Generated by software containing ST-Developer
 * from STEP Tools, Inc. (www.steptools.com) 
 */

FILE_DESCRIPTION(
/* description */ ('XY cross-slide table'),
/* implementation_level */ '2;1');

FILE_NAME(
/* name */ 'Cap Screw - M5x20.step',
/* time_stamp */ '2026-10-28T03:22:46-07:00',
/* author */ (''),
/* organization */ (''),
/* preprocessor_version */ 'ST-DEVELOPER v20.2',
/* originating_system */ 'Autodesk Translation Framework v15.17.0.0',
/* authorisation */ '');

FILE_SCHEMA (('AUTOMOTIVE_DESIGN { 1 0 10303 214 3 1 1 }'));
ENDSEC;

DATA;
#10=MECHANICAL_DESIGN_GEOMETRIC_PRESENTATION_REPRESENTATION('',(#1716),#62984);
#21=ORIENTED_CLOSED_SHELL('',*,#23013,.F.);
#30=BREP_WITH_VOIDS('Body1',#23012,(#21));
#1457=CONICAL_SURFACE('',#24826,0.4,0.785398163397448);
#1458=CONICAL_SURFACE('',#24830,0.41,0.785398163397448);
#1459=CONICAL_SURFACE('',#24834,0.26,0.463647609000806);
#1460=CONICAL_SURFACE('',#24838,0.225,0.785398163397448);
#1535=SHAPE_REPRESENTATION_RELATIONSHIP('SRR','None',#63387,#1618);
#1618=ADVANCED_BREP_SHAPE_REPRESENTATION('',(#30),#62924);
#1716=STYLED_ITEM('',(#63919),#30);
#2060=FACE_BOUND('',#4769,.T.);
#2506=PLANE('',#24824);
#2507=PLANE('',#24832);
#2508=PLANE('',#24840);
#2509=PLANE('',#24841);
#2510=PLANE('',#24842);
#2511=PLANE('',#24843);
#2512=PLANE('',#24844);
#2513=PLANE('',#24845);
#2514=PLANE('',#24846);
#2515=PLANE('',#24847);
#2516=PLANE('',#24848);
#3277=FACE_OUTER_BOUND('',#4764,.T.);
#3278=FACE_OUTER_BOUND('',#4765,.T.);
#3279=FACE_OUTER_BOUND('',#4766,.T.);
#3280=FACE_OUTER_BOUND('',#4767,.T.);
#3281=FACE_OUTER_BOUND('',#4768,.T.);
#3282=FACE_OUTER_BOUND('',#4770,.T.);
#3283=FACE_OUTER_BOUND('',#4771,.T.);
#3284=FACE_OUTER_BOUND('',#4772,.T.);
#3285=FACE_OUTER_BOUND('',#4773,.T.);
#3286=FACE_OUTER_BOUND('',#4774,.T.);
#3287=FACE_OUTER_BOUND('',#4775,.T.);
#3288=FACE_OUTER_BOUND('',#4776,.T.);
#3289=FACE_OUTER_BOUND('',#4777,.T.);
#3290=FACE_OUTER_BOUND('',#4778,.T.);
#3291=FACE_OUTER_BOUND('',#4779,.T.);
#3292=FACE_OUTER_BOUND('',#4780,.T.);
#3293=FACE_OUTER_BOUND('',#4781,.T.);
#4764=EDGE_LOOP('',(#16734));
#4765=EDGE_LOOP('',(#16735,#16736,#16737,#16738));
#4766=EDGE_LOOP('',(#16739,#16740,#16741,#16742));
#4767=EDGE_LOOP('',(#16743,#16744,#16745,#16746));
#4768=EDGE_LOOP('',(#16747));
#4769=EDGE_LOOP('',(#16748));
#4770=EDGE_LOOP('',(#16749,#16750,#16751,#16752));
#4771=EDGE_LOOP('',(#16753,#16754,#16755,#16756));
#4772=EDGE_LOOP('',(#16757,#16758,#16759,#16760));
#4773=EDGE_LOOP('',(#16761));
#4774=EDGE_LOOP('',(#16762,#16763,#16764,#16765));
#4775=EDGE_LOOP('',(#16766,#16767,#16768,#16769));
#4776=EDGE_LOOP('',(#16770,#16771,#16772,#16773));
#4777=EDGE_LOOP('',(#16774,#16775,#16776,#16777));
#4778=EDGE_LOOP('',(#16778,#16779,#16780,#16781));
#4779=EDGE_LOOP('',(#16782,#16783,#16784,#16785));
#4780=EDGE_LOOP('',(#16786,#16787,#16788,#16789,#16790,#16791));
#4781=EDGE_LOOP('',(#16792,#16793,#16794,#16795,#16796,#16797));
#6380=LINE('',#37534,#7867);
#6381=LINE('',#37538,#7868);
#6382=LINE('',#37542,#7869);
#6383=LINE('',#37549,#7870);
#6384=LINE('',#37553,#7871);
#6385=LINE('',#37557,#7872);
#6386=LINE('',#37562,#7873);
#6387=LINE('',#37564,#7874);
#6388=LINE('',#37566,#7875);
#6389=LINE('',#37567,#7876);
#6390=LINE('',#37570,#7877);
#6391=LINE('',#37572,#7878);
#6392=LINE('',#37573,#7879);
#6393=LINE('',#37576,#7880);
#6394=LINE('',#37578,#7881);
#6395=LINE('',#37579,#7882);
#6396=LINE('',#37582,#7883);
#6397=LINE('',#37584,#7884);
#6398=LINE('',#37585,#7885);
#6399=LINE('',#37588,#7886);
#6400=LINE('',#37590,#7887);
#6401=LINE('',#37591,#7888);
#6402=LINE('',#37593,#7889);
#6403=LINE('',#37594,#7890);
#7867=VECTOR('',#28591,0.4);
#7868=VECTOR('',#28596,0.425);
#7869=VECTOR('',#28601,0.41);
#7870=VECTOR('',#28610,0.26);
#7871=VECTOR('',#28615,0.25);
#7872=VECTOR('',#28620,0.225);
#7873=VECTOR('',#28625,1.);
#7874=VECTOR('',#28626,1.);
#7875=VECTOR('',#28627,1.);
#7876=VECTOR('',#28628,1.);
#7877=VECTOR('',#28631,1.);
#7878=VECTOR('',#28632,1.);
#7879=VECTOR('',#28633,1.);
#7880=VECTOR('',#28636,1.);
#7881=VECTOR('',#28637,1.);
#7882=VECTOR('',#28638,1.);
#7883=VECTOR('',#28641,1.);
#7884=VECTOR('',#28642,1.);
#7885=VECTOR('',#28643,1.);
#7886=VECTOR('',#28646,1.);
#7887=VECTOR('',#28647,1.);
#7888=VECTOR('',#28648,1.);
#7889=VECTOR('',#28651,1.);
#7890=VECTOR('',#28652,1.);
#9246=CIRCLE('',#24825,0.375);
#9247=CIRCLE('',#24827,0.425);
#9248=CIRCLE('',#24829,0.425);
#9249=CIRCLE('',#24831,0.395);
#9250=CIRCLE('',#24833,0.27);
#9251=CIRCLE('',#24835,0.24505);
#9252=CIRCLE('',#24837,0.24505);
#9253=CIRCLE('',#24839,0.2);
#10395=VERTEX_POINT('',#37529);
#10396=VERTEX_POINT('',#37532);
#10397=VERTEX_POINT('',#37536);
#10398=VERTEX_POINT('',#37540);
#10399=VERTEX_POINT('',#37544);
#10400=VERTEX_POINT('',#37547);
#10401=VERTEX_POINT('',#37551);
#10402=VERTEX_POINT('',#37555);
#10403=VERTEX_POINT('',#37560);
#10404=VERTEX_POINT('',#37561);
#10405=VERTEX_POINT('',#37563);
#10406=VERTEX_POINT('',#37565);
#10407=VERTEX_POINT('',#37569);
#10408=VERTEX_POINT('',#37571);
#10409=VERTEX_POINT('',#37575);
#10410=VERTEX_POINT('',#37577);
#10411=VERTEX_POINT('',#37581);
#10412=VERTEX_POINT('',#37583);
#10413=VERTEX_POINT('',#37587);
#10414=VERTEX_POINT('',#37589);
#12751=EDGE_CURVE('',#10395,#10395,#9246,.T.);
#12752=EDGE_CURVE('',#10396,#10396,#9247,.T.);
#12753=EDGE_CURVE('',#10396,#10395,#6380,.T.);
#12754=EDGE_CURVE('',#10397,#10397,#9248,.T.);
#12755=EDGE_CURVE('',#10397,#10396,#6381,.T.);
#12756=EDGE_CURVE('',#10398,#10398,#9249,.T.);
#12757=EDGE_CURVE('',#10398,#10397,#6382,.T.);
#12758=EDGE_CURVE('',#10399,#10399,#9250,.T.);
#12759=EDGE_CURVE('',#10400,#10400,#9251,.F.);
#12760=EDGE_CURVE('',#10400,#10399,#6383,.T.);
#12761=EDGE_CURVE('',#10401,#10401,#9252,.F.);
#12762=EDGE_CURVE('',#10401,#10400,#6384,.T.);
#12763=EDGE_CURVE('',#10402,#10402,#9253,.T.);
#12764=EDGE_CURVE('',#10402,#10401,#6385,.T.);
#12765=EDGE_CURVE('',#10403,#10404,#6386,.T.);
#12766=EDGE_CURVE('',#10404,#10405,#6387,.T.);
#12767=EDGE_CURVE('',#10405,#10406,#6388,.T.);
#12768=EDGE_CURVE('',#10403,#10406,#6389,.T.);
#12769=EDGE_CURVE('',#10404,#10407,#6390,.T.);
#12770=EDGE_CURVE('',#10407,#10408,#6391,.T.);
#12771=EDGE_CURVE('',#10408,#10405,#6392,.T.);
#12772=EDGE_CURVE('',#10407,#10409,#6393,.T.);
#12773=EDGE_CURVE('',#10409,#10410,#6394,.T.);
#12774=EDGE_CURVE('',#10410,#10408,#6395,.T.);
#12775=EDGE_CURVE('',#10409,#10411,#6396,.T.);
#12776=EDGE_CURVE('',#10411,#10412,#6397,.T.);
#12777=EDGE_CURVE('',#10412,#10410,#6398,.T.);
#12778=EDGE_CURVE('',#10411,#10413,#6399,.T.);
#12779=EDGE_CURVE('',#10413,#10414,#6400,.T.);
#12780=EDGE_CURVE('',#10414,#10412,#6401,.T.);
#12781=EDGE_CURVE('',#10413,#10403,#6402,.T.);
#12782=EDGE_CURVE('',#10406,#10414,#6403,.T.);
#16734=ORIENTED_EDGE('',*,*,#12751,.F.);
#16735=ORIENTED_EDGE('',*,*,#12752,.F.);
#16736=ORIENTED_EDGE('',*,*,#12753,.T.);
#16737=ORIENTED_EDGE('',*,*,#12751,.T.);
#16738=ORIENTED_EDGE('',*,*,#12753,.F.);
#16739=ORIENTED_EDGE('',*,*,#12754,.F.);
#16740=ORIENTED_EDGE('',*,*,#12755,.T.);
#16741=ORIENTED_EDGE('',*,*,#12752,.T.);
#16742=ORIENTED_EDGE('',*,*,#12755,.F.);
#16743=ORIENTED_EDGE('',*,*,#12756,.F.);
#16744=ORIENTED_EDGE('',*,*,#12757,.T.);
#16745=ORIENTED_EDGE('',*,*,#12754,.T.);
#16746=ORIENTED_EDGE('',*,*,#12757,.F.);
#16747=ORIENTED_EDGE('',*,*,#12756,.T.);
#16748=ORIENTED_EDGE('',*,*,#12758,.F.);
#16749=ORIENTED_EDGE('',*,*,#12759,.F.);
#16750=ORIENTED_EDGE('',*,*,#12760,.T.);
#16751=ORIENTED_EDGE('',*,*,#12758,.T.);
#16752=ORIENTED_EDGE('',*,*,#12760,.F.);
#16753=ORIENTED_EDGE('',*,*,#12761,.F.);
#16754=ORIENTED_EDGE('',*,*,#12762,.T.);
#16755=ORIENTED_EDGE('',*,*,#12759,.T.);
#16756=ORIENTED_EDGE('',*,*,#12762,.F.);
#16757=ORIENTED_EDGE('',*,*,#12763,.F.);
#16758=ORIENTED_EDGE('',*,*,#12764,.T.);
#16759=ORIENTED_EDGE('',*,*,#12761,.T.);
#16760=ORIENTED_EDGE('',*,*,#12764,.F.);
#16761=ORIENTED_EDGE('',*,*,#12763,.T.);
#16762=ORIENTED_EDGE('',*,*,#12765,.T.);
#16763=ORIENTED_EDGE('',*,*,#12766,.T.);
#16764=ORIENTED_EDGE('',*,*,#12767,.T.);
#16765=ORIENTED_EDGE('',*,*,#12768,.F.);
#16766=ORIENTED_EDGE('',*,*,#12769,.T.);
#16767=ORIENTED_EDGE('',*,*,#12770,.T.);
#16768=ORIENTED_EDGE('',*,*,#12771,.T.);
#16769=ORIENTED_EDGE('',*,*,#12766,.F.);
#16770=ORIENTED_EDGE('',*,*,#12772,.T.);
#16771=ORIENTED_EDGE('',*,*,#12773,.T.);
#16772=ORIENTED_EDGE('',*,*,#12774,.T.);
#16773=ORIENTED_EDGE('',*,*,#12770,.F.);
#16774=ORIENTED_EDGE('',*,*,#12775,.T.);
#16775=ORIENTED_EDGE('',*,*,#12776,.T.);
#16776=ORIENTED_EDGE('',*,*,#12777,.T.);
#16777=ORIENTED_EDGE('',*,*,#12773,.F.);
#16778=ORIENTED_EDGE('',*,*,#12778,.T.);
#16779=ORIENTED_EDGE('',*,*,#12779,.T.);
#16780=ORIENTED_EDGE('',*,*,#12780,.T.);
#16781=ORIENTED_EDGE('',*,*,#12776,.F.);
#16782=ORIENTED_EDGE('',*,*,#12781,.T.);
#16783=ORIENTED_EDGE('',*,*,#12768,.T.);
#16784=ORIENTED_EDGE('',*,*,#12782,.T.);
#16785=ORIENTED_EDGE('',*,*,#12779,.F.);
#16786=ORIENTED_EDGE('',*,*,#12781,.F.);
#16787=ORIENTED_EDGE('',*,*,#12778,.F.);
#16788=ORIENTED_EDGE('',*,*,#12775,.F.);
#16789=ORIENTED_EDGE('',*,*,#12772,.F.);
#16790=ORIENTED_EDGE('',*,*,#12769,.F.);
#16791=ORIENTED_EDGE('',*,*,#12765,.F.);
#16792=ORIENTED_EDGE('',*,*,#12782,.F.);
#16793=ORIENTED_EDGE('',*,*,#12767,.F.);
#16794=ORIENTED_EDGE('',*,*,#12771,.F.);
#16795=ORIENTED_EDGE('',*,*,#12774,.F.);
#16796=ORIENTED_EDGE('',*,*,#12777,.F.);
#16797=ORIENTED_EDGE('',*,*,#12780,.F.);
#21186=CYLINDRICAL_SURFACE('',#24828,0.425);
#21187=CYLINDRICAL_SURFACE('',#24836,0.24505);
#22058=ADVANCED_FACE('',(#3277),#2506,.T.);
#22059=ADVANCED_FACE('',(#3278),#1457,.T.);
#22060=ADVANCED_FACE('',(#3279),#21186,.T.);
#22061=ADVANCED_FACE('',(#3280),#1458,.T.);
#22062=ADVANCED_FACE('',(#3281,#2060),#2507,.T.);
#22063=ADVANCED_FACE('',(#3282),#1459,.T.);
#22064=ADVANCED_FACE('',(#3283),#21187,.T.);
#22065=ADVANCED_FACE('',(#3284),#1460,.T.);
#22066=ADVANCED_FACE('',(#3285),#2508,.T.);
#22067=ADVANCED_FACE('',(#3286),#2509,.F.);
#22068=ADVANCED_FACE('',(#3287),#2510,.F.);
#22069=ADVANCED_FACE('',(#3288),#2511,.F.);
#22070=ADVANCED_FACE('',(#3289),#2512,.F.);
#22071=ADVANCED_FACE('',(#3290),#2513,.F.);
#22072=ADVANCED_FACE('',(#3291),#2514,.F.);
#22073=ADVANCED_FACE('',(#3292),#2515,.F.);
#22074=ADVANCED_FACE('',(#3293),#2516,.F.);
#23012=CLOSED_SHELL('',(#22058,#22059,#22060,#22061,#22062,#22063,#22064,
#22065,#22066));
#23013=CLOSED_SHELL('',(#22067,#22068,#22069,#22070,#22071,#22072,#22073,
#22074));
#24823=AXIS2_PLACEMENT_3D('',#37527,#28581,#28582);
#24824=AXIS2_PLACEMENT_3D('',#37528,#28583,#28584);
#24825=AXIS2_PLACEMENT_3D('',#37530,#28585,#28586);
#24826=AXIS2_PLACEMENT_3D('',#37531,#28587,#28588);
#24827=AXIS2_PLACEMENT_3D('',#37533,#28589,#28590);
#24828=AXIS2_PLACEMENT_3D('',#37535,#28592,#28593);
#24829=AXIS2_PLACEMENT_3D('',#37537,#28594,#28595);
#24830=AXIS2_PLACEMENT_3D('',#37539,#28597,#28598);
#24831=AXIS2_PLACEMENT_3D('',#37541,#28599,#28600);
#24832=AXIS2_PLACEMENT_3D('',#37543,#28602,#28603);
#24833=AXIS2_PLACEMENT_3D('',#37545,#28604,#28605);
#24834=AXIS2_PLACEMENT_3D('',#37546,#28606,#28607);
#24835=AXIS2_PLACEMENT_3D('',#37548,#28608,#28609);
#24836=AXIS2_PLACEMENT_3D('',#37550,#28611,#28612);
#24837=AXIS2_PLACEMENT_3D('',#37552,#28613,#28614);
#24838=AXIS2_PLACEMENT_3D('',#37554,#28616,#28617);
#24839=AXIS2_PLACEMENT_3D('',#37556,#28618,#28619);
#24840=AXIS2_PLACEMENT_3D('',#37558,#28621,#28622);
#24841=AXIS2_PLACEMENT_3D('',#37559,#28623,#28624);
#24842=AXIS2_PLACEMENT_3D('',#37568,#28629,#28630);
#24843=AXIS2_PLACEMENT_3D('',#37574,#28634,#28635);
#24844=AXIS2_PLACEMENT_3D('',#37580,#28639,#28640);
#24845=AXIS2_PLACEMENT_3D('',#37586,#28644,#28645);
#24846=AXIS2_PLACEMENT_3D('',#37592,#28649,#28650);
#24847=AXIS2_PLACEMENT_3D('',#37595,#28653,#28654);
#24848=AXIS2_PLACEMENT_3D('',#37596,#28655,#28656);
#28581=DIRECTION('axis',(0.,0.,1.));
#28582=DIRECTION('refdir',(1.,0.,0.));
#28583=DIRECTION('center_axis',(0.,1.,0.));
#28584=DIRECTION('ref_axis',(0.,0.,1.));
#28585=DIRECTION('center_axis',(0.,-1.,0.));
#28586=DIRECTION('ref_axis',(1.,0.,0.));
#28587=DIRECTION('center_axis',(0.,-1.,0.));
#28588=DIRECTION('ref_axis',(1.,0.,0.));
#28589=DIRECTION('center_axis',(0.,-1.,0.));
#28590=DIRECTION('ref_axis',(1.,0.,0.));
#28591=DIRECTION('',(0.707106781186548,0.707106781186547,8.65956056235493E-17));
#28592=DIRECTION('center_axis',(0.,-1.,0.));
#28593=DIRECTION('ref_axis',(1.,0.,0.));
#28594=DIRECTION('center_axis',(0.,-1.,0.));
#28595=DIRECTION('ref_axis',(1.,0.,0.));
#28596=DIRECTION('',(0.,1.,0.));
#28597=DIRECTION('center_axis',(0.,1.,0.));
#28598=DIRECTION('ref_axis',(1.,0.,0.));
#28599=DIRECTION('center_axis',(0.,-1.,0.));
#28600=DIRECTION('ref_axis',(1.,0.,0.));
#28601=DIRECTION('',(-0.707106781186547,0.707106781186548,-8.65956056235493E-17));
#28602=DIRECTION('center_axis',(0.,-1.,0.));
#28603=DIRECTION('ref_axis',(0.,0.,-1.));
#28604=DIRECTION('center_axis',(0.,-1.,0.));
#28605=DIRECTION('ref_axis',(1.,0.,0.));
#28606=DIRECTION('center_axis',(0.,1.,0.));
#28607=DIRECTION('ref_axis',(1.,0.,0.));
#28608=DIRECTION('center_axis',(0.,1.,0.));
#28609=DIRECTION('ref_axis',(1.,0.,0.));
#28610=DIRECTION('',(-0.447213595499958,0.894427190999916,-5.47678698264203E-17));
#28611=DIRECTION('center_axis',(0.,-1.,0.));
#28612=DIRECTION('ref_axis',(1.,0.,0.));
#28613=DIRECTION('center_axis',(0.,1.,0.));
#28614=DIRECTION('ref_axis',(1.,0.,0.));
#28615=DIRECTION('',(0.,1.,0.));
#28616=DIRECTION('center_axis',(0.,1.,0.));
#28617=DIRECTION('ref_axis',(1.,0.,0.));
#28618=DIRECTION('center_axis',(0.,-1.,0.));
#28619=DIRECTION('ref_axis',(1.,0.,0.));
#28620=DIRECTION('',(-0.707106781186547,0.707106781186548,-8.65956056235493E-17));
#28621=DIRECTION('center_axis',(0.,-1.,0.));
#28622=DIRECTION('ref_axis',(0.,0.,-1.));
#28623=DIRECTION('center_axis',(0.866025403784439,0.,-0.5));
#28624=DIRECTION('ref_axis',(0.5,0.,0.866025403784439));
#28625=DIRECTION('',(-0.5,0.,-0.866025403784439));
#28626=DIRECTION('',(0.,-1.,0.));
#28627=DIRECTION('',(0.5,0.,0.866025403784439));
#28628=DIRECTION('',(0.,-1.,0.));
#28629=DIRECTION('center_axis',(1.20185167898973E-16,0.,-1.));
#28630=DIRECTION('ref_axis',(1.,0.,1.20185167898973E-16));
#28631=DIRECTION('',(-1.,0.,-1.20185167898973E-16));
#28632=DIRECTION('',(0.,-1.,0.));
#28633=DIRECTION('',(1.,0.,1.20185167898973E-16));
#28634=DIRECTION('center_axis',(-0.866025403784439,0.,-0.5));
#28635=DIRECTION('ref_axis',(0.5,0.,-0.866025403784439));
#28636=DIRECTION('',(-0.5,0.,0.866025403784439));
#28637=DIRECTION('',(0.,-1.,0.));
#28638=DIRECTION('',(0.5,0.,-0.866025403784439));
#28639=DIRECTION('center_axis',(-0.866025403784439,0.,0.5));
#28640=DIRECTION('ref_axis',(-0.5,0.,-0.866025403784439));
#28641=DIRECTION('',(0.5,0.,0.866025403784439));
#28642=DIRECTION('',(0.,-1.,0.));
#28643=DIRECTION('',(-0.5,0.,-0.866025403784439));
#28644=DIRECTION('center_axis',(-2.40370335797945E-16,0.,1.));
#28645=DIRECTION('ref_axis',(-1.,0.,-2.40370335797945E-16));
#28646=DIRECTION('',(1.,0.,2.40370335797945E-16));
#28647=DIRECTION('',(0.,-1.,0.));
#28648=DIRECTION('',(-1.,0.,-2.40370335797945E-16));
#28649=DIRECTION('center_axis',(0.866025403784439,0.,0.5));
#28650=DIRECTION('ref_axis',(-0.5,0.,0.866025403784439));
#28651=DIRECTION('',(0.5,0.,-0.866025403784439));
#28652=DIRECTION('',(-0.5,0.,0.866025403784439));
#28653=DIRECTION('center_axis',(0.,1.,0.));
#28654=DIRECTION('ref_axis',(1.,0.,0.));
#28655=DIRECTION('center_axis',(0.,-1.,0.));
#28656=DIRECTION('ref_axis',(0.,0.,-1.));
#37527=CARTESIAN_POINT('',(0.,0.,0.));
#37528=CARTESIAN_POINT('Origin',(0.375,0.5,0.));
#37529=CARTESIAN_POINT('',(-0.375,0.5,-4.59242549680257E-17));
#37530=CARTESIAN_POINT('Origin',(0.,0.5,0.));
#37531=CARTESIAN_POINT('Origin',(0.,0.475,0.));
#37532=CARTESIAN_POINT('',(-0.425,0.45,-5.20474889637625E-17));
#37533=CARTESIAN_POINT('Origin',(0.,0.45,0.));
#37534=CARTESIAN_POINT('',(-0.4,0.475,-4.89858719658941E-17));
#37535=CARTESIAN_POINT('Origin',(0.,0.24,0.));
#37536=CARTESIAN_POINT('',(-0.425,0.0299999999999998,-5.20474889637625E-17));
#37537=CARTESIAN_POINT('Origin',(0.,0.0299999999999998,0.));
#37538=CARTESIAN_POINT('',(-0.425,0.24,-5.20474889637625E-17));
#37539=CARTESIAN_POINT('Origin',(0.,0.0150000000000001,0.));
#37540=CARTESIAN_POINT('',(-0.395,4.85722573273506E-17,-4.83735485663204E-17));
#37541=CARTESIAN_POINT('Origin',(0.,0.,0.));
#37542=CARTESIAN_POINT('',(-0.41,0.0150000000000001,-5.02105187650415E-17));
#37543=CARTESIAN_POINT('Origin',(0.27,0.,0.));
#37544=CARTESIAN_POINT('',(-0.27,0.,-3.30654635769785E-17));
#37545=CARTESIAN_POINT('Origin',(0.,0.,0.));
#37546=CARTESIAN_POINT('Origin',(0.,-0.02,0.));
#37547=CARTESIAN_POINT('',(-0.24505,-0.0498999999999999,3.00099698131059E-17));
#37548=CARTESIAN_POINT('Origin',(0.,-0.0498999999999999,0.));
#37549=CARTESIAN_POINT('',(-0.26,-0.02,-3.18408167778312E-17));
#37550=CARTESIAN_POINT('Origin',(0.,-0.995,0.));
#37551=CARTESIAN_POINT('',(-0.24505,-1.95495,3.00099698131059E-17));
#37552=CARTESIAN_POINT('Origin',(0.,-1.95495,0.));
#37553=CARTESIAN_POINT('',(-0.24505,-0.995,-3.00099698131059E-17));
#37554=CARTESIAN_POINT('Origin',(0.,-1.975,0.));
#37555=CARTESIAN_POINT('',(-0.2,-2.,-2.44929359829471E-17));
#37556=CARTESIAN_POINT('Origin',(0.,-2.,0.));
#37557=CARTESIAN_POINT('',(-0.225,-1.975,-2.75545529808154E-17));
#37558=CARTESIAN_POINT('Origin',(0.,-2.,0.));
#37559=CARTESIAN_POINT('Origin',(0.115470053837925,-0.5,-0.2));
#37560=CARTESIAN_POINT('',(0.23094010767585,-0.5,0.));
#37561=CARTESIAN_POINT('',(0.115470053837925,-0.5,-0.2));
#37562=CARTESIAN_POINT('',(0.23094010767585,-0.5,0.));
#37563=CARTESIAN_POINT('',(0.115470053837925,-0.8,-0.2));
#37564=CARTESIAN_POINT('',(0.115470053837925,-0.5,-0.2));
#37565=CARTESIAN_POINT('',(0.23094010767585,-0.8,0.));
#37566=CARTESIAN_POINT('',(0.23094010767585,-0.8,0.));
#37567=CARTESIAN_POINT('',(0.23094010767585,-0.5,0.));
#37568=CARTESIAN_POINT('Origin',(-0.115470053837925,-0.5,-0.2));
#37569=CARTESIAN_POINT('',(-0.115470053837925,-0.5,-0.2));
#37570=CARTESIAN_POINT('',(0.115470053837925,-0.5,-0.2));
#37571=CARTESIAN_POINT('',(-0.115470053837925,-0.8,-0.2));
#37572=CARTESIAN_POINT('',(-0.115470053837925,-0.5,-0.2));
#37573=CARTESIAN_POINT('',(0.115470053837925,-0.8,-0.2));
#37574=CARTESIAN_POINT('Origin',(-0.23094010767585,-0.5,-2.77555756156289E-17));
#37575=CARTESIAN_POINT('',(-0.23094010767585,-0.5,-2.82820063659975E-17));
#37576=CARTESIAN_POINT('',(-0.115470053837925,-0.5,-0.2));
#37577=CARTESIAN_POINT('',(-0.23094010767585,-0.8,-2.77555756156289E-17));
#37578=CARTESIAN_POINT('',(-0.23094010767585,-0.5,-2.82820063659975E-17));
#37579=CARTESIAN_POINT('',(-0.115470053837925,-0.8,-0.2));
#37580=CARTESIAN_POINT('Origin',(-0.115470053837925,-0.5,0.2));
#37581=CARTESIAN_POINT('',(-0.115470053837925,-0.5,0.2));
#37582=CARTESIAN_POINT('',(-0.23094010767585,-0.5,-2.82820063659975E-17));
#37583=CARTESIAN_POINT('',(-0.115470053837925,-0.8,0.2));
#37584=CARTESIAN_POINT('',(-0.115470053837925,-0.5,0.2));
#37585=CARTESIAN_POINT('',(-0.23094010767585,-0.8,-2.82820063659975E-17));
#37586=CARTESIAN_POINT('Origin',(0.115470053837925,-0.5,0.2));
#37587=CARTESIAN_POINT('',(0.115470053837925,-0.5,0.2));
#37588=CARTESIAN_POINT('',(-0.115470053837925,-0.5,0.2));
#37589=CARTESIAN_POINT('',(0.115470053837925,-0.8,0.2));
#37590=CARTESIAN_POINT('',(0.115470053837925,-0.5,0.2));
#37591=CARTESIAN_POINT('',(-0.115470053837925,-0.8,0.2));
#37592=CARTESIAN_POINT('Origin',(0.23094010767585,-0.5,0.));
#37593=CARTESIAN_POINT('',(0.115470053837925,-0.5,0.2));
#37594=CARTESIAN_POINT('',(0.115470053837925,-0.8,0.2));
#37595=CARTESIAN_POINT('Origin',(0.,-0.5,0.));
#37596=CARTESIAN_POINT('Origin',(0.,-0.8,0.));
#62825=UNCERTAINTY_MEASURE_WITH_UNIT(LENGTH_MEASURE(0.001),#62985,
'DISTANCE_ACCURACY_VALUE',
'Maximum model space distance between geometric entities at asserted c
onnectivities');
#62885=UNCERTAINTY_MEASURE_WITH_UNIT(LENGTH_MEASURE(0.001),#62985,
'DISTANCE_ACCURACY_VALUE',
'Maximum model space distance between geometric entities at asserted c
onnectivities');
#62924=(
GEOMETRIC_REPRESENTATION_CONTEXT(3)
GLOBAL_UNCERTAINTY_ASSIGNED_CONTEXT((#62825))
GLOBAL_UNIT_ASSIGNED_CONTEXT((#62985,#62987,#62988))
REPRESENTATION_CONTEXT('','3D')
);
#62984=(
GEOMETRIC_REPRESENTATION_CONTEXT(3)
GLOBAL_UNCERTAINTY_ASSIGNED_CONTEXT((#62885))
GLOBAL_UNIT_ASSIGNED_CONTEXT((#62985,#62987,#62988))
REPRESENTATION_CONTEXT('','3D')
);
#62985=(
LENGTH_UNIT()
NAMED_UNIT(*)
SI_UNIT(.CENTI.,.METRE.)
);
#62987=(
NAMED_UNIT(*)
PLANE_ANGLE_UNIT()
SI_UNIT($,.RADIAN.)
);
#62988=(
NAMED_UNIT(*)
SI_UNIT($,.STERADIAN.)
SOLID_ANGLE_UNIT()
);
#63027=SHAPE_DEFINITION_REPRESENTATION(#63138,#63387);
#63138=PRODUCT_DEFINITION_SHAPE('',$,#63486);
#63387=SHAPE_REPRESENTATION('',(#24823),#62924);
#63447=PRODUCT_DEFINITION_CONTEXT('part definition',#63743,'design');
#63486=PRODUCT_DEFINITION('Cap Screw - M5x20','Cap Screw - M5x20',#63584,
#63447);
#63584=PRODUCT_DEFINITION_FORMATION('',$,#63783);
#63743=APPLICATION_CONTEXT(
'Core Data for Automotive Mechanical Design Process');
#63744=PRODUCT_CONTEXT('part definition',#63743,'mechanical');
#63783=PRODUCT('Cap Screw - M5x20','Cap Screw - M5x20',
'Cap Screw - M5x20',(#63744));
#63913=COLOUR_RGB('Black',0.12,0.14,0.17);
#63914=FILL_AREA_STYLE_COLOUR('',#63913);
#63915=FILL_AREA_STYLE('',(#63914));
#63916=SURFACE_STYLE_FILL_AREA(#63915);
#63917=SURFACE_SIDE_STYLE('',(#63916));
#63918=SURFACE_STYLE_USAGE(.BOTH.,#63917);
#63919=PRESENTATION_STYLE_ASSIGNMENT((#63918));
ENDSEC;
END-ISO-10303-21;
